ISO-10303-21;
HEADER;
/* Generated by software containing ST-Developer
 * from STEP Tools, Inc. (www.steptools.com) 
 */

FILE_DESCRIPTION(
/* description */ ('PAT-072'),
/* implementation_level */ '2;1');

FILE_NAME(
/* name */ 'Gallery closure (1).step',
/* time_stamp */ '2026-10-29T20:11:56-07:00',
/* author */ (''),
/* organization */ (''),
/* preprocessor_version */ 'ST-DEVELOPER v20.2',
/* originating_system */ 'Autodesk Translation Framework v15.17.0.0',
/* authorisation */ '');

FILE_SCHEMA (('AUTOMOTIVE_DESIGN { 1 0 10303 214 3 1 1 }'));
ENDSEC;

DATA;
#10=MECHANICAL_DESIGN_GEOMETRIC_PRESENTATION_REPRESENTATION('',(#349),#11432);
#277=SHAPE_REPRESENTATION_RELATIONSHIP('SRR','None',#11581,#313);
#313=ADVANCED_BREP_SHAPE_REPRESENTATION('',(#385),#11412);
#349=STYLED_ITEM('',(#11812),#385);
#385=MANIFOLD_SOLID_BREP('Body1',#6084);
#655=PLANE('',#6830);
#656=PLANE('',#6831);
#956=FACE_OUTER_BOUND('',#1410,.T.);
#957=FACE_OUTER_BOUND('',#1411,.T.);
#958=FACE_OUTER_BOUND('',#1412,.T.);
#1410=EDGE_LOOP('',(#4672,#4673,#4674,#4675));
#1411=EDGE_LOOP('',(#4676));
#1412=EDGE_LOOP('',(#4677));
#1839=LINE('',#10214,#2258);
#2258=VECTOR('',#8044,0.3);
#2685=CIRCLE('',#6828,0.3);
#2686=CIRCLE('',#6829,0.3);
#3034=VERTEX_POINT('',#10211);
#3035=VERTEX_POINT('',#10213);
#3625=EDGE_CURVE('',#3034,#3034,#2685,.T.);
#3626=EDGE_CURVE('',#3034,#3035,#1839,.T.);
#3627=EDGE_CURVE('',#3035,#3035,#2686,.T.);
#4672=ORIENTED_EDGE('',*,*,#3625,.F.);
#4673=ORIENTED_EDGE('',*,*,#3626,.T.);
#4674=ORIENTED_EDGE('',*,*,#3627,.T.);
#4675=ORIENTED_EDGE('',*,*,#3626,.F.);
#4676=ORIENTED_EDGE('',*,*,#3625,.T.);
#4677=ORIENTED_EDGE('',*,*,#3627,.F.);
#5633=CYLINDRICAL_SURFACE('',#6827,0.3);
#5855=ADVANCED_FACE('',(#956),#5633,.T.);
#5856=ADVANCED_FACE('',(#957),#655,.T.);
#5857=ADVANCED_FACE('',(#958),#656,.F.);
#6084=CLOSED_SHELL('',(#5855,#5856,#5857));
#6826=AXIS2_PLACEMENT_3D('',#10209,#8038,#8039);
#6827=AXIS2_PLACEMENT_3D('',#10210,#8040,#8041);
#6828=AXIS2_PLACEMENT_3D('',#10212,#8042,#8043);
#6829=AXIS2_PLACEMENT_3D('',#10215,#8045,#8046);
#6830=AXIS2_PLACEMENT_3D('',#10216,#8047,#8048);
#6831=AXIS2_PLACEMENT_3D('',#10217,#8049,#8050);
#8038=DIRECTION('axis',(0.,0.,1.));
#8039=DIRECTION('refdir',(1.,0.,0.));
#8040=DIRECTION('center_axis',(1.,0.,0.));
#8041=DIRECTION('ref_axis',(0.,0.,-1.));
#8042=DIRECTION('center_axis',(1.,0.,0.));
#8043=DIRECTION('ref_axis',(0.,0.,-1.));
#8044=DIRECTION('',(-1.,0.,0.));
#8045=DIRECTION('center_axis',(1.,0.,0.));
#8046=DIRECTION('ref_axis',(0.,0.,-1.));
#8047=DIRECTION('center_axis',(1.,0.,0.));
#8048=DIRECTION('ref_axis',(0.,0.,-1.));
#8049=DIRECTION('center_axis',(1.,0.,0.));
#8050=DIRECTION('ref_axis',(0.,0.,-1.));
#10209=CARTESIAN_POINT('',(0.,0.,0.));
#10210=CARTESIAN_POINT('Origin',(5.1,1.5,4.));
#10211=CARTESIAN_POINT('',(5.5,1.5,4.3));
#10212=CARTESIAN_POINT('Origin',(5.5,1.5,4.));
#10213=CARTESIAN_POINT('',(5.1,1.5,4.3));
#10214=CARTESIAN_POINT('',(5.1,1.5,4.3));
#10215=CARTESIAN_POINT('Origin',(5.1,1.5,4.));
#10216=CARTESIAN_POINT('Origin',(5.5,1.5,4.));
#10217=CARTESIAN_POINT('Origin',(5.1,1.5,4.));
#11373=UNCERTAINTY_MEASURE_WITH_UNIT(LENGTH_MEASURE(0.001),#11433,
'DISTANCE_ACCURACY_VALUE',
'Maximum model space distance between geometric entities at asserted c
onnectivities');
#11393=UNCERTAINTY_MEASURE_WITH_UNIT(LENGTH_MEASURE(0.001),#11433,
'DISTANCE_ACCURACY_VALUE',
'Maximum model space distance between geometric entities at asserted c
onnectivities');
#11412=(
GEOMETRIC_REPRESENTATION_CONTEXT(3)
GLOBAL_UNCERTAINTY_ASSIGNED_CONTEXT((#11373))
GLOBAL_UNIT_ASSIGNED_CONTEXT((#11433,#11435,#11436))
REPRESENTATION_CONTEXT('','3D')
);
#11432=(
GEOMETRIC_REPRESENTATION_CONTEXT(3)
GLOBAL_UNCERTAINTY_ASSIGNED_CONTEXT((#11393))
GLOBAL_UNIT_ASSIGNED_CONTEXT((#11433,#11435,#11436))
REPRESENTATION_CONTEXT('','3D')
);
#11433=(
LENGTH_UNIT()
NAMED_UNIT(*)
SI_UNIT(.CENTI.,.METRE.)
);
#11435=(
NAMED_UNIT(*)
PLANE_ANGLE_UNIT()
SI_UNIT($,.RADIAN.)
);
#11436=(
NAMED_UNIT(*)
SI_UNIT($,.STERADIAN.)
SOLID_ANGLE_UNIT()
);
#11455=SHAPE_DEFINITION_REPRESENTATION(#11493,#11581);
#11493=PRODUCT_DEFINITION_SHAPE('',$,#11620);
#11581=SHAPE_REPRESENTATION('',(#6826),#11412);
#11601=PRODUCT_DEFINITION_CONTEXT('part definition',#11717,'design');
#11620=PRODUCT_DEFINITION('Gallery closure (1)',
'Gallery closure (1)',#11658,#11601);
#11658=PRODUCT_DEFINITION_FORMATION('',$,#11737);
#11717=APPLICATION_CONTEXT(
'Core Data for Automotive Mechanical Design Process');
#11718=PRODUCT_CONTEXT('part definition',#11717,'mechanical');
#11737=PRODUCT('Gallery closure (1)','Gallery closure (1)',
'Gallery closure (1)',(#11718));
#11806=COLOUR_RGB('Sky Blue',0.24,0.69,0.87);
#11807=FILL_AREA_STYLE_COLOUR('',#11806);
#11808=FILL_AREA_STYLE('',(#11807));
#11809=SURFACE_STYLE_FILL_AREA(#11808);
#11810=SURFACE_SIDE_STYLE('',(#11809));
#11811=SURFACE_STYLE_USAGE(.BOTH.,#11810);
#11812=PRESENTATION_STYLE_ASSIGNMENT((#11811));
ENDSEC;
END-ISO-10303-21;
